ISO-10303-21;
HEADER;
/* Generated by software containing ST-Developer
 * from STEP Tools, Inc. (www.steptools.com) 
 */

FILE_DESCRIPTION(
/* description */ ('Cam-driven reciprocating slide'),
/* implementation_level */ '2;1');

FILE_NAME(
/* name */ 'Axial keeper (1).step',
/* time_stamp */ '2026-10-28T03:25:20-07:00',
/* author */ (''),
/* organization */ (''),
/* preprocessor_version */ 'ST-DEVELOPER v20.2',
/* originating_system */ 'Autodesk Translation Framework v15.17.0.0',
/* authorisation */ '');

FILE_SCHEMA (('AUTOMOTIVE_DESIGN { 1 0 10303 214 3 1 1 }'));
ENDSEC;

DATA;
#10=MECHANICAL_DESIGN_GEOMETRIC_PRESENTATION_REPRESENTATION('',(#460),#13277);
#379=SHAPE_REPRESENTATION_RELATIONSHIP('SRR','None',#13475,#416);
#416=ADVANCED_BREP_SHAPE_REPRESENTATION('',(#502),#13270);
#460=STYLED_ITEM('',(#13706),#502);
#502=MANIFOLD_SOLID_BREP('Body1',#6438);
#664=FACE_BOUND('',#1763,.T.);
#665=FACE_BOUND('',#1765,.T.);
#862=PLANE('',#7519);
#863=PLANE('',#7520);
#1224=FACE_OUTER_BOUND('',#1760,.T.);
#1225=FACE_OUTER_BOUND('',#1761,.T.);
#1226=FACE_OUTER_BOUND('',#1762,.T.);
#1227=FACE_OUTER_BOUND('',#1764,.T.);
#1760=EDGE_LOOP('',(#5666,#5667,#5668,#5669));
#1761=EDGE_LOOP('',(#5670,#5671,#5672,#5673));
#1762=EDGE_LOOP('',(#5674));
#1763=EDGE_LOOP('',(#5675));
#1764=EDGE_LOOP('',(#5676));
#1765=EDGE_LOOP('',(#5677));
#2189=LINE('',#12881,#2628);
#2190=LINE('',#12887,#2629);
#2628=VECTOR('',#9349,0.225);
#2629=VECTOR('',#9356,1.);
#3005=CIRCLE('',#7514,0.225);
#3006=CIRCLE('',#7515,0.225);
#3007=CIRCLE('',#7517,1.);
#3008=CIRCLE('',#7518,1.);
#3484=VERTEX_POINT('',#12878);
#3485=VERTEX_POINT('',#12880);
#3486=VERTEX_POINT('',#12884);
#3487=VERTEX_POINT('',#12886);
#4223=EDGE_CURVE('',#3484,#3484,#3005,.T.);
#4224=EDGE_CURVE('',#3484,#3485,#2189,.T.);
#4225=EDGE_CURVE('',#3485,#3485,#3006,.T.);
#4226=EDGE_CURVE('',#3486,#3486,#3007,.T.);
#4227=EDGE_CURVE('',#3486,#3487,#2190,.T.);
#4228=EDGE_CURVE('',#3487,#3487,#3008,.T.);
#5666=ORIENTED_EDGE('',*,*,#4223,.F.);
#5667=ORIENTED_EDGE('',*,*,#4224,.T.);
#5668=ORIENTED_EDGE('',*,*,#4225,.T.);
#5669=ORIENTED_EDGE('',*,*,#4224,.F.);
#5670=ORIENTED_EDGE('',*,*,#4226,.F.);
#5671=ORIENTED_EDGE('',*,*,#4227,.T.);
#5672=ORIENTED_EDGE('',*,*,#4228,.T.);
#5673=ORIENTED_EDGE('',*,*,#4227,.F.);
#5674=ORIENTED_EDGE('',*,*,#4226,.T.);
#5675=ORIENTED_EDGE('',*,*,#4223,.T.);
#5676=ORIENTED_EDGE('',*,*,#4228,.F.);
#5677=ORIENTED_EDGE('',*,*,#4225,.F.);
#6006=CYLINDRICAL_SURFACE('',#7513,0.225);
#6007=CYLINDRICAL_SURFACE('',#7516,1.);
#6342=ADVANCED_FACE('',(#1224),#6006,.F.);
#6343=ADVANCED_FACE('',(#1225),#6007,.T.);
#6344=ADVANCED_FACE('',(#1226,#664),#862,.T.);
#6345=ADVANCED_FACE('',(#1227,#665),#863,.F.);
#6438=CLOSED_SHELL('',(#6342,#6343,#6344,#6345));
#7512=AXIS2_PLACEMENT_3D('',#12876,#9343,#9344);
#7513=AXIS2_PLACEMENT_3D('',#12877,#9345,#9346);
#7514=AXIS2_PLACEMENT_3D('',#12879,#9347,#9348);
#7515=AXIS2_PLACEMENT_3D('',#12882,#9350,#9351);
#7516=AXIS2_PLACEMENT_3D('',#12883,#9352,#9353);
#7517=AXIS2_PLACEMENT_3D('',#12885,#9354,#9355);
#7518=AXIS2_PLACEMENT_3D('',#12888,#9357,#9358);
#7519=AXIS2_PLACEMENT_3D('',#12889,#9359,#9360);
#7520=AXIS2_PLACEMENT_3D('',#12890,#9361,#9362);
#9343=DIRECTION('axis',(0.,0.,1.));
#9344=DIRECTION('refdir',(1.,0.,0.));
#9345=DIRECTION('center_axis',(0.,1.,0.));
#9346=DIRECTION('ref_axis',(1.,0.,0.));
#9347=DIRECTION('center_axis',(0.,-1.,0.));
#9348=DIRECTION('ref_axis',(1.,0.,0.));
#9349=DIRECTION('',(0.,-1.,0.));
#9350=DIRECTION('center_axis',(0.,-1.,0.));
#9351=DIRECTION('ref_axis',(1.,0.,0.));
#9352=DIRECTION('center_axis',(0.,1.,0.));
#9353=DIRECTION('ref_axis',(1.,0.,0.));
#9354=DIRECTION('center_axis',(0.,1.,0.));
#9355=DIRECTION('ref_axis',(1.,0.,0.));
#9356=DIRECTION('',(0.,-1.,0.));
#9357=DIRECTION('center_axis',(0.,1.,0.));
#9358=DIRECTION('ref_axis',(1.,0.,0.));
#9359=DIRECTION('center_axis',(0.,1.,0.));
#9360=DIRECTION('ref_axis',(1.,0.,0.));
#9361=DIRECTION('center_axis',(0.,1.,0.));
#9362=DIRECTION('ref_axis',(1.,0.,0.));
#12876=CARTESIAN_POINT('',(0.,0.,0.));
#12877=CARTESIAN_POINT('Origin',(0.,6.5,4.));
#12878=CARTESIAN_POINT('',(-0.225,6.7,4.));
#12879=CARTESIAN_POINT('Origin',(0.,6.7,4.));
#12880=CARTESIAN_POINT('',(-0.225,6.5,4.));
#12881=CARTESIAN_POINT('',(-0.225,6.5,4.));
#12882=CARTESIAN_POINT('Origin',(0.,6.5,4.));
#12883=CARTESIAN_POINT('Origin',(0.,6.5,4.));
#12884=CARTESIAN_POINT('',(-1.,6.7,4.));
#12885=CARTESIAN_POINT('Origin',(0.,6.7,4.));
#12886=CARTESIAN_POINT('',(-1.,6.5,4.));
#12887=CARTESIAN_POINT('',(-1.,6.5,4.));
#12888=CARTESIAN_POINT('Origin',(0.,6.5,4.));
#12889=CARTESIAN_POINT('Origin',(0.,6.7,4.));
#12890=CARTESIAN_POINT('Origin',(0.,6.5,4.));
#13226=UNCERTAINTY_MEASURE_WITH_UNIT(LENGTH_MEASURE(0.001),#13278,
'DISTANCE_ACCURACY_VALUE',
'Maximum model space distance between geometric entities at asserted c
onnectivities');
#13233=UNCERTAINTY_MEASURE_WITH_UNIT(LENGTH_MEASURE(0.001),#13278,
'DISTANCE_ACCURACY_VALUE',
'Maximum model space distance between geometric entities at asserted c
onnectivities');
#13270=(
GEOMETRIC_REPRESENTATION_CONTEXT(3)
GLOBAL_UNCERTAINTY_ASSIGNED_CONTEXT((#13226))
GLOBAL_UNIT_ASSIGNED_CONTEXT((#13278,#13280,#13281))
REPRESENTATION_CONTEXT('','3D')
);
#13277=(
GEOMETRIC_REPRESENTATION_CONTEXT(3)
GLOBAL_UNCERTAINTY_ASSIGNED_CONTEXT((#13233))
GLOBAL_UNIT_ASSIGNED_CONTEXT((#13278,#13280,#13281))
REPRESENTATION_CONTEXT('','3D')
);
#13278=(
LENGTH_UNIT()
NAMED_UNIT(*)
SI_UNIT(.CENTI.,.METRE.)
);
#13280=(
NAMED_UNIT(*)
PLANE_ANGLE_UNIT()
SI_UNIT($,.RADIAN.)
);
#13281=(
NAMED_UNIT(*)
SI_UNIT($,.STERADIAN.)
SOLID_ANGLE_UNIT()
);
#13318=SHAPE_DEFINITION_REPRESENTATION(#13368,#13475);
#13368=PRODUCT_DEFINITION_SHAPE('',$,#13519);
#13475=SHAPE_REPRESENTATION('',(#7512),#13270);
#13482=PRODUCT_DEFINITION_CONTEXT('part definition',#13613,'design');
#13519=PRODUCT_DEFINITION('Axial keeper (1)','Axial keeper (1)',#13562,#13482);
#13562=PRODUCT_DEFINITION_FORMATION('',$,#13651);
#13613=APPLICATION_CONTEXT(
'Core Data for Automotive Mechanical Design Process');
#13614=PRODUCT_CONTEXT('part definition',#13613,'mechanical');
#13651=PRODUCT('Axial keeper (1)','Axial keeper (1)','Axial keeper (1)',(#13614));
#13700=COLOUR_RGB('Light Blue',0.38,0.62,0.78);
#13701=FILL_AREA_STYLE_COLOUR('',#13700);
#13702=FILL_AREA_STYLE('',(#13701));
#13703=SURFACE_STYLE_FILL_AREA(#13702);
#13704=SURFACE_SIDE_STYLE('',(#13703));
#13705=SURFACE_STYLE_USAGE(.BOTH.,#13704);
#13706=PRESENTATION_STYLE_ASSIGNMENT((#13705));
ENDSEC;
END-ISO-10303-21;
